ISO-10303-21;
HEADER;
FILE_DESCRIPTION (('STEP AP203'),
    '1' );
FILE_NAME ('1602p_c_10.step',
    '2026-10-31T14:11:27',
    ( '' ),
    ( '' ),
    'SwSTEP 2.0',
    'SolidWorks 2024',
    '' );
FILE_SCHEMA (( 'AUTOMOTIVE_DESIGN' ));
ENDSEC;

DATA;
#349=CYLINDRICAL_SURFACE ( 'NONE', #19361, 3.499999999999998668 ) ;
#350=EDGE_CURVE ( 'NONE', #15518, #357, #2469, .T. ) ;
#357=VERTEX_POINT ( 'NONE', #13631 ) ;
#415=DIRECTION ( 'NONE',  ( 1.000000000000000000, 0.000000000000000000, 0.000000000000000000 ) ) ;
#742=CARTESIAN_POINT ( 'NONE',  ( -19.49999999982360066, -0.1021026942259700004, 2.500000000000000000 ) ) ;
#888=ORIENTED_EDGE ( 'NONE', *, *, #14022, .T. ) ;
#1075=ORIENTED_EDGE ( 'NONE', *, *, #11246, .F. ) ;
#1233=MANIFOLD_SOLID_BREP ( 'Imported1', #6874 ) ;
#1323=FACE_BOUND ( 'NONE', #15873, .T. ) ;
#1449=CARTESIAN_POINT ( 'NONE',  ( -22.99995202268966921, -0.1204285676209190525, 2.500000000000000444 ) ) ;
#1530=PRODUCT_DEFINITION ( 'UNKNOWN', '', #1997, #14428 ) ;
#1598=CARTESIAN_POINT ( 'NONE',  ( -19.49999999982360066, -0.1021026942259700004, -1.101737663870589950E-14 ) ) ;
#1778=ADVANCED_FACE ( 'NONE', ( #5595 ), #349, .T. ) ;
#1952=DIRECTION ( 'NONE',  ( -1.187319687680494078E-16, -2.805478249478255076E-20, -1.000000000000000000 ) ) ;
#1997=PRODUCT_DEFINITION_FORMATION_WITH_SPECIFIED_SOURCE ( 'ANY', '', #18416, .NOT_KNOWN. ) ;
#2100=DIRECTION ( 'NONE',  ( -1.187319687680494078E-16, -2.805478249478260493E-20, -1.000000000000000000 ) ) ;
#2309=DIRECTION ( 'NONE',  ( 1.187319687680494078E-16, 2.805478249478255076E-20, 1.000000000000000000 ) ) ;
#2343=ADVANCED_FACE ( 'NONE', ( #10785 ), #5280, .F. ) ;
#2439=LINE ( 'NONE', #9694, #22667 ) ;
#2469=CIRCLE ( 'NONE', #13848, 2.499999999999998224 ) ;
#2569=CARTESIAN_POINT ( 'NONE',  ( 0.000000000000000000, 0.000000000000000000, 0.000000000000000000 ) ) ;
#2729=CARTESIAN_POINT ( 'NONE',  ( -22.99995202268966921, -0.1204285676209190525, -2.499999999999999556 ) ) ;
#2758=CARTESIAN_POINT ( 'NONE',  ( -19.49999999982360066, -0.1021026942259700004, -2.500000000000000000 ) ) ;
#2789=DIRECTION ( 'NONE',  ( -1.187319687680494078E-16, -2.805478249478275539E-20, -1.000000000000000000 ) ) ;
#3251=ORIENTED_EDGE ( 'NONE', *, *, #10708, .T. ) ;
#3270=( GEOMETRIC_REPRESENTATION_CONTEXT ( 3 ) GLOBAL_UNCERTAINTY_ASSIGNED_CONTEXT ( ( #14645 ) ) GLOBAL_UNIT_ASSIGNED_CONTEXT ( ( #20005, #6972, #14072 ) ) REPRESENTATION_CONTEXT ( 'NONE', 'WORKASPACE' ) );
#3296=ADVANCED_FACE ( 'NONE', ( #19930 ), #22043, .F. ) ;
#3375=SHAPE_REPRESENTATION_RELATIONSHIP ( 'NONE' , 'NONE' ,  #12659, #4822 ) ;
#3407=DIRECTION ( 'NONE',  ( 1.187319687680494078E-16, 2.805478249478275539E-20, 1.000000000000000000 ) ) ;
#3545=CARTESIAN_POINT ( 'NONE',  ( -19.49999999982360066, -0.1021026942259700004, -2.500000000000000000 ) ) ;
#3834=CARTESIAN_POINT ( 'NONE',  ( -19.49999999982360066, -0.1021026942259700004, -2.500000000000000000 ) ) ;
#4135=SHAPE_DEFINITION_REPRESENTATION ( #18992, #12659 ) ;
#4146=ORIENTED_EDGE ( 'NONE', *, *, #10459, .F. ) ;
#4442=DIRECTION ( 'NONE',  ( -1.187319687680494078E-16, -2.805478249478275539E-20, -1.000000000000000000 ) ) ;
#4667=DIRECTION ( 'NONE',  ( -1.187319687680499994E-16, -2.805478249478560216E-20, -1.000000000000000000 ) ) ;
#4822=ADVANCED_BREP_SHAPE_REPRESENTATION ( '', ( #1233, #12739 ), #3270 ) ;
#5095=AXIS2_PLACEMENT_3D ( 'NONE', #15121, #4442, #22593 ) ;
#5280=CYLINDRICAL_SURFACE ( 'NONE', #15390, 2.499999999999998224 ) ;
#5595=FACE_OUTER_BOUND ( 'NONE', #14048, .T. ) ;
#5843=DIRECTION ( 'NONE',  ( -1.187319687680494078E-16, -2.805478249478265308E-20, -1.000000000000000000 ) ) ;
#5997=ORIENTED_EDGE ( 'NONE', *, *, #350, .T. ) ;
#6229=ADVANCED_FACE ( 'NONE', ( #1323, #21271 ), #10612, .F. ) ;
#6855=ORIENTED_EDGE ( 'NONE', *, *, #19571, .F. ) ;
#6874=CLOSED_SHELL ( 'NONE', ( #1778, #2343, #3296, #6229, #18004, #20671 ) ) ;
#6878=DIRECTION ( 'NONE',  ( -0.9999862922474491711, -0.005235963827128302210, 1.239088197126291310E-16 ) ) ;
#6901=AXIS2_PLACEMENT_3D ( 'NONE', #3545, #8772, #6878 ) ;
#6972=( NAMED_UNIT ( * ) PLANE_ANGLE_UNIT ( ) SI_UNIT ( $, .RADIAN. ) );
#7007=CIRCLE ( 'NONE', #5095, 3.499999999999998668 ) ;
#7024=APPLICATION_CONTEXT ( 'configuration controlled 3d designs of mechanical parts and assemblies' ) ;
#7115=ORIENTED_EDGE ( 'NONE', *, *, #19571, .T. ) ;
#7129=ORIENTED_EDGE ( 'NONE', *, *, #10588, .T. ) ;
#7175=EDGE_LOOP ( 'NONE', ( #17826, #18204, #1075, #6855 ) ) ;
#7274=CIRCLE ( 'NONE', #6901, 3.499999999999998668 ) ;
#7373=VECTOR ( 'NONE', #9204, 1000.000000000000000 ) ;
#7468=ORIENTED_EDGE ( 'NONE', *, *, #8199, .F. ) ;
#8199=EDGE_CURVE ( 'NONE', #17821, #19182, #11953, .T. ) ;
#8315=ORIENTED_EDGE ( 'NONE', *, *, #15468, .T. ) ;
#8333=DIRECTION ( 'NONE',  ( -0.9999862922474491711, -0.005235963827128305680, 1.734723475976808327E-16 ) ) ;
#8772=DIRECTION ( 'NONE',  ( 1.187319687680494078E-16, 2.805478249478275539E-20, 1.000000000000000000 ) ) ;
#8897=ORIENTED_EDGE ( 'NONE', *, *, #8964, .F. ) ;
#8904=FACE_OUTER_BOUND ( 'NONE', #20203, .T. ) ;
#8964=EDGE_CURVE ( 'NONE', #20644, #19182, #9320, .T. ) ;
#9076=EDGE_CURVE ( 'NONE', #20644, #9363, #7007, .T. ) ;
#9152=ORIENTED_EDGE ( 'NONE', *, *, #11334, .F. ) ;
#9204=DIRECTION ( 'NONE',  ( -1.187319687680494078E-16, -2.805478249478265308E-20, -1.000000000000000000 ) ) ;
#9320=LINE ( 'NONE', #21784, #7373 ) ;
#9363=VERTEX_POINT ( 'NONE', #1449 ) ;
#9389=AXIS2_PLACEMENT_3D ( 'NONE', #2758, #19262, #8333 ) ;
#9404=CARTESIAN_POINT ( 'NONE',  ( -19.49999999982360066, -0.1021026942259700004, -1.101737663870589950E-14 ) ) ;
#9694=CARTESIAN_POINT ( 'NONE',  ( -22.99995202268966921, -0.1204285676209190525, -1.060181993030890135E-14 ) ) ;
#10459=EDGE_CURVE ( 'NONE', #357, #15518, #16712, .T. ) ;
#10577=DIRECTION ( 'NONE',  ( -0.9999862922474491711, -0.005235963827128302210, 1.187304881134281446E-16 ) ) ;
#10588=EDGE_CURVE ( 'NONE', #14947, #11330, #17493, .T. ) ;
#10612=PLANE ( 'NONE',  #12132 ) ;
#10654=DIRECTION ( 'NONE',  ( -1.187319687680494078E-16, -2.805478249478260493E-20, -1.000000000000000000 ) ) ;
#10708=EDGE_CURVE ( 'NONE', #9363, #20644, #15977, .T. ) ;
#10785=FACE_OUTER_BOUND ( 'NONE', #7175, .T. ) ;
#10929=ORIENTED_EDGE ( 'NONE', *, *, #11246, .T. ) ;
#11246=EDGE_CURVE ( 'NONE', #11330, #14947, #21141, .T. ) ;
#11330=VERTEX_POINT ( 'NONE', #17718 ) ;
#11334=EDGE_CURVE ( 'NONE', #15518, #14947, #17256, .T. ) ;
#11517=AXIS2_PLACEMENT_3D ( 'NONE', #3834, #19763, #21646 ) ;
#11562=ORIENTED_EDGE ( 'NONE', *, *, #9076, .F. ) ;
#11810=CARTESIAN_POINT ( 'NONE',  ( -21.99996573044222004, -0.1151926037937907599, -1.072055041842232962E-14 ) ) ;
#11953=CIRCLE ( 'NONE', #15273, 3.499999999999998668 ) ;
#12045=LINE ( 'NONE', #11810, #13037 ) ;
#12046=AXIS2_PLACEMENT_3D ( 'NONE', #12914, #2100, #18035 ) ;
#12093=ORIENTED_EDGE ( 'NONE', *, *, #8199, .T. ) ;
#12132=AXIS2_PLACEMENT_3D ( 'NONE', #14158, #4667, #17615 ) ;
#12550=ORIENTED_EDGE ( 'NONE', *, *, #8964, .T. ) ;
#12659=SHAPE_REPRESENTATION ( '1602p_c_10', ( #12739 ), #3270 ) ;
#12739=AXIS2_PLACEMENT_3D ( 'NONE', #2569, #13380, #415 ) ;
#12914=CARTESIAN_POINT ( 'NONE',  ( -19.49999999982360066, -0.1021026942259700004, -1.101737663870589950E-14 ) ) ;
#12989=PLANE ( 'NONE',  #11517 ) ;
#13037=VECTOR ( 'NONE', #15818, 1000.000000000000000 ) ;
#13070=AXIS2_PLACEMENT_3D ( 'NONE', #13996, #21121, #10577 ) ;
#13091=DIRECTION ( 'NONE',  ( -0.9999862922474491711, -0.005235963827128302210, 1.187304881134281446E-16 ) ) ;
#13157=EDGE_LOOP ( 'NONE', ( #7468, #13915 ) ) ;
#13380=DIRECTION ( 'NONE',  ( 0.000000000000000000, 0.000000000000000000, 1.000000000000000000 ) ) ;
#13631=CARTESIAN_POINT ( 'NONE',  ( -21.99996573044222004, -0.1151926037937907599, 2.500000000000000444 ) ) ;
#13711=ORIENTED_EDGE ( 'NONE', *, *, #9076, .T. ) ;
#13805=CARTESIAN_POINT ( 'NONE',  ( -17.00003426920497773, -0.08901278465814893570, -1.131420285898946938E-14 ) ) ;
#13842=FACE_OUTER_BOUND ( 'NONE', #13157, .T. ) ;
#13848=AXIS2_PLACEMENT_3D ( 'NONE', #15404, #21103, #15525 ) ;
#13875=CARTESIAN_POINT ( 'NONE',  ( -19.49999999982360066, -0.1021026942259700004, -2.500000000000000000 ) ) ;
#13915=ORIENTED_EDGE ( 'NONE', *, *, #15468, .F. ) ;
#13996=CARTESIAN_POINT ( 'NONE',  ( -19.49999999982360066, -0.1021026942259700004, -1.101737663870589950E-14 ) ) ;
#14022=EDGE_CURVE ( 'NONE', #9363, #17821, #2439, .T. ) ;
#14030=AXIS2_PLACEMENT_3D ( 'NONE', #18593, #2309, #17278 ) ;
#14048=EDGE_LOOP ( 'NONE', ( #3251, #12550, #8315, #16001 ) ) ;
#14072=( NAMED_UNIT ( * ) SI_UNIT ( $, .STERADIAN. ) SOLID_ANGLE_UNIT ( ) );
#14105=DIRECTION ( 'NONE',  ( -0.9999862922474491711, -0.005235963827128302210, 1.239088197126291310E-16 ) ) ;
#14158=CARTESIAN_POINT ( 'NONE',  ( -19.49999999982360066, -0.1021026942259700004, 2.500000000000000000 ) ) ;
#14239=ORIENTED_EDGE ( 'NONE', *, *, #10708, .F. ) ;
#14428=DESIGN_CONTEXT ( 'detailed design', #17476, 'design' ) ;
#14645=UNCERTAINTY_MEASURE_WITH_UNIT (LENGTH_MEASURE( 1.000000000000000082E-05 ), #20005, 'distance_accuracy_value', 'NONE');
#14947=VERTEX_POINT ( 'NONE', #21386 ) ;
#15121=CARTESIAN_POINT ( 'NONE',  ( -19.49999999982360066, -0.1021026942259700004, 2.500000000000000000 ) ) ;
#15273=AXIS2_PLACEMENT_3D ( 'NONE', #13875, #3407, #14105 ) ;
#15390=AXIS2_PLACEMENT_3D ( 'NONE', #1598, #10654, #17882 ) ;
#15404=CARTESIAN_POINT ( 'NONE',  ( -19.49999999982360066, -0.1021026942259700004, 2.500000000000000000 ) ) ;
#15468=EDGE_CURVE ( 'NONE', #19182, #17821, #7274, .T. ) ;
#15518=VERTEX_POINT ( 'NONE', #23248 ) ;
#15523=EDGE_LOOP ( 'NONE', ( #14239, #11562 ) ) ;
#15525=DIRECTION ( 'NONE',  ( -0.9999862922474491711, -0.005235963827128305680, 1.734723475976808327E-16 ) ) ;
#15818=DIRECTION ( 'NONE',  ( -1.187319687680494078E-16, -2.805478249478260493E-20, -1.000000000000000000 ) ) ;
#15873=EDGE_LOOP ( 'NONE', ( #19807, #5997 ) ) ;
#15961=CARTESIAN_POINT ( 'NONE',  ( -16.00004797695752501, -0.08377682083102050425, 2.499999999999999556 ) ) ;
#15977=CIRCLE ( 'NONE', #19023, 3.499999999999998668 ) ;
#16001=ORIENTED_EDGE ( 'NONE', *, *, #14022, .F. ) ;
#16274=EDGE_LOOP ( 'NONE', ( #9152, #4146, #7115, #18691 ) ) ;
#16712=CIRCLE ( 'NONE', #19762, 2.499999999999998224 ) ;
#16956=MECHANICAL_CONTEXT ( 'NONE', #7024, 'mechanical' ) ;
#17150=DIRECTION ( 'NONE',  ( -1.187319687680494078E-16, -2.805478249478265308E-20, -1.000000000000000000 ) ) ;
#17153=DIRECTION ( 'NONE',  ( -0.9999862922474491711, -0.005235963827128302210, 1.239088197126291310E-16 ) ) ;
#17256=LINE ( 'NONE', #13805, #22644 ) ;
#17278=DIRECTION ( 'NONE',  ( -0.9999862922474491711, -0.005235963827128305680, 1.734723475976808327E-16 ) ) ;
#17476=APPLICATION_CONTEXT ( 'configuration controlled 3d designs of mechanical parts and assemblies' ) ;
#17493=CIRCLE ( 'NONE', #14030, 2.499999999999998224 ) ;
#17615=DIRECTION ( 'NONE',  ( -1.000000000000000000, 0.000000000000000000, 1.187319687680499994E-16 ) ) ;
#17718=CARTESIAN_POINT ( 'NONE',  ( -21.99996573044222004, -0.1151926037937907599, -2.499999999999999556 ) ) ;
#17821=VERTEX_POINT ( 'NONE', #2729 ) ;
#17826=ORIENTED_EDGE ( 'NONE', *, *, #350, .F. ) ;
#17882=DIRECTION ( 'NONE',  ( -0.9999862922474491711, -0.005235963827128305680, 1.187304881134278487E-16 ) ) ;
#18004=ADVANCED_FACE ( 'NONE', ( #8904 ), #21472, .T. ) ;
#18035=DIRECTION ( 'NONE',  ( -0.9999862922474491711, -0.005235963827128305680, 1.187304881134278487E-16 ) ) ;
#18204=ORIENTED_EDGE ( 'NONE', *, *, #11334, .T. ) ;
#18341=CARTESIAN_POINT ( 'NONE',  ( -16.00004797695752501, -0.08377682083102050425, -2.500000000000000444 ) ) ;
#18416=PRODUCT ( '1602p_c_10', '1602p_c_10', '', ( #16956 ) ) ;
#18593=CARTESIAN_POINT ( 'NONE',  ( -19.49999999982360066, -0.1021026942259700004, -2.500000000000000000 ) ) ;
#18691=ORIENTED_EDGE ( 'NONE', *, *, #10588, .F. ) ;
#18992=PRODUCT_DEFINITION_SHAPE ( 'NONE', 'NONE',  #1530 ) ;
#19023=AXIS2_PLACEMENT_3D ( 'NONE', #742, #2789, #17153 ) ;
#19182=VERTEX_POINT ( 'NONE', #18341 ) ;
#19187=FACE_BOUND ( 'NONE', #23338, .T. ) ;
#19262=DIRECTION ( 'NONE',  ( 1.187319687680494078E-16, 2.805478249478255076E-20, 1.000000000000000000 ) ) ;
#19361=AXIS2_PLACEMENT_3D ( 'NONE', #9404, #5843, #13091 ) ;
#19571=EDGE_CURVE ( 'NONE', #357, #11330, #12045, .T. ) ;
#19762=AXIS2_PLACEMENT_3D ( 'NONE', #23446, #1952, #19779 ) ;
#19763=DIRECTION ( 'NONE',  ( -1.187319687680499994E-16, -2.805478249478560216E-20, -1.000000000000000000 ) ) ;
#19779=DIRECTION ( 'NONE',  ( -0.9999862922474491711, -0.005235963827128305680, 1.734723475976808327E-16 ) ) ;
#19807=ORIENTED_EDGE ( 'NONE', *, *, #10459, .T. ) ;
#19930=FACE_OUTER_BOUND ( 'NONE', #16274, .T. ) ;
#20005=( LENGTH_UNIT ( ) NAMED_UNIT ( * ) SI_UNIT ( .MILLI., .METRE. ) );
#20203=EDGE_LOOP ( 'NONE', ( #8897, #13711, #888, #12093 ) ) ;
#20644=VERTEX_POINT ( 'NONE', #15961 ) ;
#20671=ADVANCED_FACE ( 'NONE', ( #19187, #13842 ), #12989, .T. ) ;
#21103=DIRECTION ( 'NONE',  ( -1.187319687680494078E-16, -2.805478249478255076E-20, -1.000000000000000000 ) ) ;
#21121=DIRECTION ( 'NONE',  ( -1.187319687680494078E-16, -2.805478249478265308E-20, -1.000000000000000000 ) ) ;
#21141=CIRCLE ( 'NONE', #9389, 2.499999999999998224 ) ;
#21271=FACE_OUTER_BOUND ( 'NONE', #15523, .T. ) ;
#21386=CARTESIAN_POINT ( 'NONE',  ( -17.00003426920497418, -0.08901278465814893570, -2.500000000000000444 ) ) ;
#21472=CYLINDRICAL_SURFACE ( 'NONE', #13070, 3.499999999999998668 ) ;
#21646=DIRECTION ( 'NONE',  ( -1.000000000000000000, 0.000000000000000000, 1.187319687680499994E-16 ) ) ;
#21784=CARTESIAN_POINT ( 'NONE',  ( -16.00004797695752856, -0.08377682083102051813, -1.143293334710289765E-14 ) ) ;
#22043=CYLINDRICAL_SURFACE ( 'NONE', #12046, 2.499999999999998224 ) ;
#22593=DIRECTION ( 'NONE',  ( -0.9999862922474491711, -0.005235963827128302210, 1.239088197126291310E-16 ) ) ;
#22644=VECTOR ( 'NONE', #22684, 1000.000000000000000 ) ;
#22667=VECTOR ( 'NONE', #17150, 1000.000000000000000 ) ;
#22684=DIRECTION ( 'NONE',  ( -1.187319687680494078E-16, -2.805478249478260493E-20, -1.000000000000000000 ) ) ;
#23248=CARTESIAN_POINT ( 'NONE',  ( -17.00003426920497418, -0.08901278465814893570, 2.499999999999999556 ) ) ;
#23338=EDGE_LOOP ( 'NONE', ( #10929, #7129 ) ) ;
#23446=CARTESIAN_POINT ( 'NONE',  ( -19.49999999982360066, -0.1021026942259700004, 2.500000000000000000 ) ) ;
#23515=COLOUR_RGB('Deep Blue', 0.09019608, 0.27058824, 0.51372549);
#23516=FILL_AREA_STYLE_COLOUR('',#23515);
#23517=FILL_AREA_STYLE('',(#23516));
#23518=SURFACE_STYLE_FILL_AREA(#23517);
#23519=SURFACE_SIDE_STYLE('',(#23518));
#23520=SURFACE_STYLE_USAGE(.BOTH.,#23519);
#23521=PRESENTATION_STYLE_ASSIGNMENT((#23520));
#23573=STYLED_ITEM('',(#23521),#1233);
#23574=MECHANICAL_DESIGN_GEOMETRIC_PRESENTATION_REPRESENTATION('',(#23573),#3270);
ENDSEC;
END-ISO-10303-21;
